ISO-10303-21;
HEADER;
/* Generated by software containing ST-Developer
 * from STEP Tools, Inc. (www.steptools.com) 
 */

FILE_DESCRIPTION(
/* description */ (''),
/* implementation_level */ '2;1');

FILE_NAME(
/* name */ 'ISO 2338 - 2 m6 x 6 - St (Carriage Travel Stop Pin).step',
/* time_stamp */ '2026-10-05T09:57:53+05:00',
/* author */ (''),
/* organization */ (''),
/* preprocessor_version */ 'ST-DEVELOPER v20.2',
/* originating_system */ 'Autodesk Translation Framework v15.15.0.0',
/* authorisation */ '');

FILE_SCHEMA (('AUTOMOTIVE_DESIGN { 1 0 10303 214 3 1 1 }'));
ENDSEC;

DATA;
#10=MECHANICAL_DESIGN_GEOMETRIC_PRESENTATION_REPRESENTATION('',(#568),#113984);
#532=SHAPE_REPRESENTATION_RELATIONSHIP('SRR','None',#114069,#550);
#550=ADVANCED_BREP_SHAPE_REPRESENTATION('',(#586),#113983);
#568=STYLED_ITEM('',(#114310),#586);
#586=MANIFOLD_SOLID_BREP(
'ISO 2338 - 2 m6 x 6 - St (Carriage Travel Stop Pin)',#60409);
#874=CYLINDRICAL_SURFACE('',#63747,1.);
#955=CONICAL_SURFACE('',#63745,0.85,0.785398163397447);
#956=CONICAL_SURFACE('',#63749,0.85,0.785398163397448);
#1538=CIRCLE('',#63744,0.7);
#1539=CIRCLE('',#63746,1.);
#1540=CIRCLE('',#63748,1.);
#1541=CIRCLE('',#63750,0.7);
#4023=PLANE('',#63743);
#4024=PLANE('',#63751);
#7287=FACE_OUTER_BOUND('',#10871,.T.);
#7288=FACE_OUTER_BOUND('',#10872,.T.);
#7289=FACE_OUTER_BOUND('',#10873,.T.);
#7290=FACE_OUTER_BOUND('',#10874,.T.);
#7291=FACE_OUTER_BOUND('',#10875,.T.);
#10871=EDGE_LOOP('',(#56399));
#10872=EDGE_LOOP('',(#56400,#56401,#56402,#56403));
#10873=EDGE_LOOP('',(#56404,#56405,#56406,#56407));
#10874=EDGE_LOOP('',(#56408,#56409,#56410,#56411));
#10875=EDGE_LOOP('',(#56412));
#16907=LINE('',#113911,#22941);
#16908=LINE('',#113915,#22942);
#16909=LINE('',#113919,#22943);
#22941=VECTOR('',#76083,0.85);
#22942=VECTOR('',#76088,1.);
#22943=VECTOR('',#76093,0.85);
#30348=VERTEX_POINT('',#113906);
#30349=VERTEX_POINT('',#113909);
#30350=VERTEX_POINT('',#113913);
#30351=VERTEX_POINT('',#113917);
#39032=EDGE_CURVE('',#30348,#30348,#1538,.T.);
#39033=EDGE_CURVE('',#30349,#30349,#1539,.T.);
#39034=EDGE_CURVE('',#30349,#30348,#16907,.T.);
#39035=EDGE_CURVE('',#30350,#30350,#1540,.T.);
#39036=EDGE_CURVE('',#30350,#30349,#16908,.T.);
#39037=EDGE_CURVE('',#30351,#30351,#1541,.T.);
#39038=EDGE_CURVE('',#30351,#30350,#16909,.T.);
#56399=ORIENTED_EDGE('',*,*,#39032,.F.);
#56400=ORIENTED_EDGE('',*,*,#39033,.F.);
#56401=ORIENTED_EDGE('',*,*,#39034,.T.);
#56402=ORIENTED_EDGE('',*,*,#39032,.T.);
#56403=ORIENTED_EDGE('',*,*,#39034,.F.);
#56404=ORIENTED_EDGE('',*,*,#39035,.F.);
#56405=ORIENTED_EDGE('',*,*,#39036,.T.);
#56406=ORIENTED_EDGE('',*,*,#39033,.T.);
#56407=ORIENTED_EDGE('',*,*,#39036,.F.);
#56408=ORIENTED_EDGE('',*,*,#39037,.F.);
#56409=ORIENTED_EDGE('',*,*,#39038,.T.);
#56410=ORIENTED_EDGE('',*,*,#39035,.T.);
#56411=ORIENTED_EDGE('',*,*,#39038,.F.);
#56412=ORIENTED_EDGE('',*,*,#39037,.T.);
#60387=ADVANCED_FACE('',(#7287),#4023,.T.);
#60388=ADVANCED_FACE('',(#7288),#955,.T.);
#60389=ADVANCED_FACE('',(#7289),#874,.T.);
#60390=ADVANCED_FACE('',(#7290),#956,.T.);
#60391=ADVANCED_FACE('',(#7291),#4024,.T.);
#60409=CLOSED_SHELL('',(#60387,#60388,#60389,#60390,#60391));
#63742=AXIS2_PLACEMENT_3D('',#113904,#76073,#76074);
#63743=AXIS2_PLACEMENT_3D('',#113905,#76075,#76076);
#63744=AXIS2_PLACEMENT_3D('',#113907,#76077,#76078);
#63745=AXIS2_PLACEMENT_3D('',#113908,#76079,#76080);
#63746=AXIS2_PLACEMENT_3D('',#113910,#76081,#76082);
#63747=AXIS2_PLACEMENT_3D('',#113912,#76084,#76085);
#63748=AXIS2_PLACEMENT_3D('',#113914,#76086,#76087);
#63749=AXIS2_PLACEMENT_3D('',#113916,#76089,#76090);
#63750=AXIS2_PLACEMENT_3D('',#113918,#76091,#76092);
#63751=AXIS2_PLACEMENT_3D('',#113920,#76094,#76095);
#76073=DIRECTION('axis',(0.,0.,1.));
#76074=DIRECTION('refdir',(1.,0.,0.));
#76075=DIRECTION('center_axis',(0.,1.,0.));
#76076=DIRECTION('ref_axis',(0.,0.,1.));
#76077=DIRECTION('center_axis',(0.,-1.,0.));
#76078=DIRECTION('ref_axis',(1.,0.,0.));
#76079=DIRECTION('center_axis',(0.,-1.,0.));
#76080=DIRECTION('ref_axis',(1.,0.,0.));
#76081=DIRECTION('center_axis',(0.,-1.,0.));
#76082=DIRECTION('ref_axis',(1.,0.,0.));
#76083=DIRECTION('',(0.707106781186547,0.707106781186548,8.65956056235493E-17));
#76084=DIRECTION('center_axis',(0.,-1.,0.));
#76085=DIRECTION('ref_axis',(1.,0.,0.));
#76086=DIRECTION('center_axis',(0.,-1.,0.));
#76087=DIRECTION('ref_axis',(1.,0.,0.));
#76088=DIRECTION('',(0.,1.,0.));
#76089=DIRECTION('center_axis',(0.,1.,0.));
#76090=DIRECTION('ref_axis',(1.,0.,0.));
#76091=DIRECTION('center_axis',(0.,-1.,0.));
#76092=DIRECTION('ref_axis',(1.,0.,0.));
#76093=DIRECTION('',(-0.707106781186548,0.707106781186547,-8.65956056235493E-17));
#76094=DIRECTION('center_axis',(0.,-1.,0.));
#76095=DIRECTION('ref_axis',(0.,0.,-1.));
#113904=CARTESIAN_POINT('',(0.,0.,0.));
#113905=CARTESIAN_POINT('Origin',(4.7,10.5,11.));
#113906=CARTESIAN_POINT('',(3.3,10.5,11.));
#113907=CARTESIAN_POINT('Origin',(4.,10.5,11.));
#113908=CARTESIAN_POINT('Origin',(4.,10.35,11.));
#113909=CARTESIAN_POINT('',(3.,10.2,11.));
#113910=CARTESIAN_POINT('Origin',(4.,10.2,11.));
#113911=CARTESIAN_POINT('',(3.15,10.35,11.));
#113912=CARTESIAN_POINT('Origin',(4.,7.5,11.));
#113913=CARTESIAN_POINT('',(3.,4.8,11.));
#113914=CARTESIAN_POINT('Origin',(4.,4.8,11.));
#113915=CARTESIAN_POINT('',(3.,7.5,11.));
#113916=CARTESIAN_POINT('Origin',(4.,4.65,11.));
#113917=CARTESIAN_POINT('',(3.3,4.5,11.));
#113918=CARTESIAN_POINT('Origin',(4.,4.5,11.));
#113919=CARTESIAN_POINT('',(3.15,4.65,11.));
#113920=CARTESIAN_POINT('Origin',(4.,4.5,11.));
#113963=UNCERTAINTY_MEASURE_WITH_UNIT(LENGTH_MEASURE(0.01),#113985,
'DISTANCE_ACCURACY_VALUE',
'Maximum model space distance between geometric entities at asserted c
onnectivities');
#113964=UNCERTAINTY_MEASURE_WITH_UNIT(LENGTH_MEASURE(0.01),#113985,
'DISTANCE_ACCURACY_VALUE',
'Maximum model space distance between geometric entities at asserted c
onnectivities');
#113983=(
GEOMETRIC_REPRESENTATION_CONTEXT(3)
GLOBAL_UNCERTAINTY_ASSIGNED_CONTEXT((#113963))
GLOBAL_UNIT_ASSIGNED_CONTEXT((#113985,#113987,#113988))
REPRESENTATION_CONTEXT('','3D')
);
#113984=(
GEOMETRIC_REPRESENTATION_CONTEXT(3)
GLOBAL_UNCERTAINTY_ASSIGNED_CONTEXT((#113964))
GLOBAL_UNIT_ASSIGNED_CONTEXT((#113985,#113987,#113988))
REPRESENTATION_CONTEXT('','3D')
);
#113985=(
LENGTH_UNIT()
NAMED_UNIT(*)
SI_UNIT(.MILLI.,.METRE.)
);
#113987=(
NAMED_UNIT(*)
PLANE_ANGLE_UNIT()
SI_UNIT($,.RADIAN.)
);
#113988=(
NAMED_UNIT(*)
SI_UNIT($,.STERADIAN.)
SOLID_ANGLE_UNIT()
);
#114007=SHAPE_DEFINITION_REPRESENTATION(#114026,#114069);
#114026=PRODUCT_DEFINITION_SHAPE('',$,#114089);
#114069=SHAPE_REPRESENTATION('',(#63742),#113983);
#114070=PRODUCT_DEFINITION_CONTEXT('part definition',#114129,'design');
#114089=PRODUCT_DEFINITION('2026-10-05-09-51-13-557',
'ISO 2338 - 2 m6 x 6 - St (Carriage Travel Stop Pin)',#114108,#114070);
#114108=PRODUCT_DEFINITION_FORMATION('',$,#114149);
#114129=APPLICATION_CONTEXT(
'Core Data for Automotive Mechanical Design Process');
#114130=PRODUCT_CONTEXT('part definition',#114129,'mechanical');
#114149=PRODUCT('2026-10-05-09-51-13-557',
'ISO 2338 - 2 m6 x 6 - St (Carriage Travel Stop Pin)',$,(#114130));
#114304=COLOUR_RGB('Grey',0.48,0.52,0.57);
#114305=FILL_AREA_STYLE_COLOUR('',#114304);
#114306=FILL_AREA_STYLE('',(#114305));
#114307=SURFACE_STYLE_FILL_AREA(#114306);
#114308=SURFACE_SIDE_STYLE('',(#114307));
#114309=SURFACE_STYLE_USAGE(.BOTH.,#114308);
#114310=PRESENTATION_STYLE_ASSIGNMENT((#114309));
ENDSEC;
END-ISO-10303-21;
